ISO-10303-21;
HEADER;
/* Generated by software containing ST-Developer
 * from STEP Tools, Inc. (www.steptools.com) 
 */

FILE_DESCRIPTION(
/* description */ ('Belt conveyor head drive unit'),
/* implementation_level */ '2;1');

FILE_NAME(
/* name */ 'Input M3 set screw (1).step',
/* time_stamp */ '2026-10-28T03:26:19-07:00',
/* author */ (''),
/* organization */ (''),
/* preprocessor_version */ 'ST-DEVELOPER v20.2',
/* originating_system */ 'Autodesk Translation Framework v15.17.0.0',
/* authorisation */ '');

FILE_SCHEMA (('AUTOMOTIVE_DESIGN { 1 0 10303 214 3 1 1 }'));
ENDSEC;

DATA;
#10=MECHANICAL_DESIGN_GEOMETRIC_PRESENTATION_REPRESENTATION('',(#911),#27069);
#757=SHAPE_REPRESENTATION_RELATIONSHIP('SRR','None',#27405,#826);
#826=ADVANCED_BREP_SHAPE_REPRESENTATION('',(#992),#27047);
#911=STYLED_ITEM('',(#27804),#992);
#992=MANIFOLD_SOLID_BREP('Body1',#13780);
#1554=PLANE('',#15691);
#1555=PLANE('',#15692);
#2171=FACE_OUTER_BOUND('',#3173,.T.);
#2172=FACE_OUTER_BOUND('',#3174,.T.);
#2173=FACE_OUTER_BOUND('',#3175,.T.);
#3173=EDGE_LOOP('',(#11226,#11227,#11228,#11229));
#3174=EDGE_LOOP('',(#11230));
#3175=EDGE_LOOP('',(#11231));
#4055=LINE('',#24529,#4847);
#4847=VECTOR('',#19247,0.15);
#5603=CIRCLE('',#15689,0.15);
#5604=CIRCLE('',#15690,0.15);
#6729=VERTEX_POINT('',#24526);
#6730=VERTEX_POINT('',#24528);
#8305=EDGE_CURVE('',#6729,#6729,#5603,.T.);
#8306=EDGE_CURVE('',#6729,#6730,#4055,.T.);
#8307=EDGE_CURVE('',#6730,#6730,#5604,.T.);
#11226=ORIENTED_EDGE('',*,*,#8305,.F.);
#11227=ORIENTED_EDGE('',*,*,#8306,.T.);
#11228=ORIENTED_EDGE('',*,*,#8307,.T.);
#11229=ORIENTED_EDGE('',*,*,#8306,.F.);
#11230=ORIENTED_EDGE('',*,*,#8305,.T.);
#11231=ORIENTED_EDGE('',*,*,#8307,.F.);
#12735=CYLINDRICAL_SURFACE('',#15688,0.15);
#13450=ADVANCED_FACE('',(#2171),#12735,.T.);
#13451=ADVANCED_FACE('',(#2172),#1554,.T.);
#13452=ADVANCED_FACE('',(#2173),#1555,.F.);
#13780=CLOSED_SHELL('',(#13450,#13451,#13452));
#15687=AXIS2_PLACEMENT_3D('',#24524,#19241,#19242);
#15688=AXIS2_PLACEMENT_3D('',#24525,#19243,#19244);
#15689=AXIS2_PLACEMENT_3D('',#24527,#19245,#19246);
#15690=AXIS2_PLACEMENT_3D('',#24530,#19248,#19249);
#15691=AXIS2_PLACEMENT_3D('',#24531,#19250,#19251);
#15692=AXIS2_PLACEMENT_3D('',#24532,#19252,#19253);
#19241=DIRECTION('axis',(0.,0.,1.));
#19242=DIRECTION('refdir',(1.,0.,0.));
#19243=DIRECTION('center_axis',(0.,0.,1.));
#19244=DIRECTION('ref_axis',(1.,0.,0.));
#19245=DIRECTION('center_axis',(0.,0.,1.));
#19246=DIRECTION('ref_axis',(1.,0.,0.));
#19247=DIRECTION('',(0.,0.,-1.));
#19248=DIRECTION('center_axis',(0.,0.,1.));
#19249=DIRECTION('ref_axis',(1.,0.,0.));
#19250=DIRECTION('center_axis',(0.,0.,1.));
#19251=DIRECTION('ref_axis',(1.,0.,0.));
#19252=DIRECTION('center_axis',(0.,0.,1.));
#19253=DIRECTION('ref_axis',(1.,0.,0.));
#24524=CARTESIAN_POINT('',(0.,0.,0.));
#24525=CARTESIAN_POINT('Origin',(0.,-3.95,7.4));
#24526=CARTESIAN_POINT('',(-0.15,-3.95,7.65));
#24527=CARTESIAN_POINT('Origin',(0.,-3.95,7.65));
#24528=CARTESIAN_POINT('',(-0.15,-3.95,7.4));
#24529=CARTESIAN_POINT('',(-0.15,-3.95,7.4));
#24530=CARTESIAN_POINT('Origin',(0.,-3.95,7.4));
#24531=CARTESIAN_POINT('Origin',(0.,-3.95,7.65));
#24532=CARTESIAN_POINT('Origin',(0.,-3.95,7.4));
#26970=UNCERTAINTY_MEASURE_WITH_UNIT(LENGTH_MEASURE(0.001),#27070,
'DISTANCE_ACCURACY_VALUE',
'Maximum model space distance between geometric entities at asserted c
onnectivities');
#26992=UNCERTAINTY_MEASURE_WITH_UNIT(LENGTH_MEASURE(0.001),#27070,
'DISTANCE_ACCURACY_VALUE',
'Maximum model space distance between geometric entities at asserted c
onnectivities');
#27047=(
GEOMETRIC_REPRESENTATION_CONTEXT(3)
GLOBAL_UNCERTAINTY_ASSIGNED_CONTEXT((#26970))
GLOBAL_UNIT_ASSIGNED_CONTEXT((#27070,#27072,#27073))
REPRESENTATION_CONTEXT('','3D')
);
#27069=(
GEOMETRIC_REPRESENTATION_CONTEXT(3)
GLOBAL_UNCERTAINTY_ASSIGNED_CONTEXT((#26992))
GLOBAL_UNIT_ASSIGNED_CONTEXT((#27070,#27072,#27073))
REPRESENTATION_CONTEXT('','3D')
);
#27070=(
LENGTH_UNIT()
NAMED_UNIT(*)
SI_UNIT(.CENTI.,.METRE.)
);
#27072=(
NAMED_UNIT(*)
PLANE_ANGLE_UNIT()
SI_UNIT($,.RADIAN.)
);
#27073=(
NAMED_UNIT(*)
SI_UNIT($,.STERADIAN.)
SOLID_ANGLE_UNIT()
);
#27128=SHAPE_DEFINITION_REPRESENTATION(#27216,#27405);
#27216=PRODUCT_DEFINITION_SHAPE('',$,#27482);
#27405=SHAPE_REPRESENTATION('',(#15687),#27047);
#27427=PRODUCT_DEFINITION_CONTEXT('part definition',#27657,'design');
#27482=PRODUCT_DEFINITION('Input M3 set screw (1)',
'Input M3 set screw (1)',#27558,#27427);
#27558=PRODUCT_DEFINITION_FORMATION('',$,#27713);
#27657=APPLICATION_CONTEXT(
'Core Data for Automotive Mechanical Design Process');
#27658=PRODUCT_CONTEXT('part definition',#27657,'mechanical');
#27713=PRODUCT('Input M3 set screw (1)','Input M3 set screw (1)',
'Input M3 set screw (1)',(#27658));
#27798=COLOUR_RGB('Black',0.12,0.14,0.17);
#27799=FILL_AREA_STYLE_COLOUR('',#27798);
#27800=FILL_AREA_STYLE('',(#27799));
#27801=SURFACE_STYLE_FILL_AREA(#27800);
#27802=SURFACE_SIDE_STYLE('',(#27801));
#27803=SURFACE_STYLE_USAGE(.BOTH.,#27802);
#27804=PRESENTATION_STYLE_ASSIGNMENT((#27803));
ENDSEC;
END-ISO-10303-21;
